ISO-10303-21;
HEADER;
/* Generated by software containing ST-Developer
 * from STEP Tools, Inc. (www.steptools.com) 
 */

FILE_DESCRIPTION(
/* description */ ('Bracket-mounted idler roller'),
/* implementation_level */ '2;1');

FILE_NAME(
/* name */ 'M6x18 mounting screw.step',
/* time_stamp */ '2026-10-28T03:26:42-07:00',
/* author */ (''),
/* organization */ (''),
/* preprocessor_version */ 'ST-DEVELOPER v20.2',
/* originating_system */ 'Autodesk Translation Framework v15.17.0.0',
/* authorisation */ '');

FILE_SCHEMA (('AUTOMOTIVE_DESIGN { 1 0 10303 214 3 1 1 }'));
ENDSEC;

DATA;
#10=MECHANICAL_DESIGN_GEOMETRIC_PRESENTATION_REPRESENTATION('',(#288),#6241);
#223=CONICAL_SURFACE('',#3577,0.475,0.785398163397449);
#224=CONICAL_SURFACE('',#3581,0.485,0.785398163397448);
#225=CONICAL_SURFACE('',#3585,0.31,0.463647609000806);
#234=ORIENTED_CLOSED_SHELL('',*,#3190,.F.);
#236=BREP_WITH_VOIDS('Body1',#3191,(#234));
#246=SHAPE_REPRESENTATION_RELATIONSHIP('SRR','None',#6350,#267);
#267=ADVANCED_BREP_SHAPE_REPRESENTATION('',(#236),#6226);
#288=STYLED_ITEM('',(#6545),#236);
#368=FACE_BOUND('',#820,.T.);
#463=PLANE('',#3565);
#464=PLANE('',#3566);
#465=PLANE('',#3567);
#466=PLANE('',#3568);
#467=PLANE('',#3569);
#468=PLANE('',#3570);
#469=PLANE('',#3571);
#470=PLANE('',#3572);
#471=PLANE('',#3573);
#472=PLANE('',#3575);
#473=PLANE('',#3583);
#583=FACE_OUTER_BOUND('',#806,.T.);
#584=FACE_OUTER_BOUND('',#807,.T.);
#585=FACE_OUTER_BOUND('',#808,.T.);
#586=FACE_OUTER_BOUND('',#809,.T.);
#587=FACE_OUTER_BOUND('',#810,.T.);
#588=FACE_OUTER_BOUND('',#811,.T.);
#589=FACE_OUTER_BOUND('',#812,.T.);
#590=FACE_OUTER_BOUND('',#813,.T.);
#591=FACE_OUTER_BOUND('',#814,.T.);
#592=FACE_OUTER_BOUND('',#815,.T.);
#593=FACE_OUTER_BOUND('',#816,.T.);
#594=FACE_OUTER_BOUND('',#817,.T.);
#595=FACE_OUTER_BOUND('',#818,.T.);
#596=FACE_OUTER_BOUND('',#819,.T.);
#597=FACE_OUTER_BOUND('',#821,.T.);
#598=FACE_OUTER_BOUND('',#822,.T.);
#806=EDGE_LOOP('',(#2436,#2437,#2438,#2439));
#807=EDGE_LOOP('',(#2440,#2441,#2442,#2443));
#808=EDGE_LOOP('',(#2444,#2445,#2446,#2447));
#809=EDGE_LOOP('',(#2448,#2449,#2450,#2451));
#810=EDGE_LOOP('',(#2452,#2453,#2454,#2455));
#811=EDGE_LOOP('',(#2456,#2457,#2458,#2459));
#812=EDGE_LOOP('',(#2460,#2461,#2462,#2463,#2464,#2465));
#813=EDGE_LOOP('',(#2466,#2467,#2468,#2469,#2470,#2471));
#814=EDGE_LOOP('',(#2472));
#815=EDGE_LOOP('',(#2473));
#816=EDGE_LOOP('',(#2474,#2475,#2476,#2477));
#817=EDGE_LOOP('',(#2478,#2479,#2480,#2481));
#818=EDGE_LOOP('',(#2482,#2483,#2484,#2485));
#819=EDGE_LOOP('',(#2486));
#820=EDGE_LOOP('',(#2487));
#821=EDGE_LOOP('',(#2488,#2489,#2490,#2491));
#822=EDGE_LOOP('',(#2492,#2493,#2494,#2495));
#1072=LINE('',#5256,#1254);
#1073=LINE('',#5258,#1255);
#1074=LINE('',#5260,#1256);
#1075=LINE('',#5261,#1257);
#1076=LINE('',#5264,#1258);
#1077=LINE('',#5266,#1259);
#1078=LINE('',#5267,#1260);
#1079=LINE('',#5270,#1261);
#1080=LINE('',#5272,#1262);
#1081=LINE('',#5273,#1263);
#1082=LINE('',#5276,#1264);
#1083=LINE('',#5278,#1265);
#1084=LINE('',#5279,#1266);
#1085=LINE('',#5282,#1267);
#1086=LINE('',#5284,#1268);
#1087=LINE('',#5285,#1269);
#1088=LINE('',#5287,#1270);
#1089=LINE('',#5288,#1271);
#1090=LINE('',#5300,#1272);
#1091=LINE('',#5304,#1273);
#1092=LINE('',#5308,#1274);
#1093=LINE('',#5315,#1275);
#1094=LINE('',#5317,#1276);
#1254=VECTOR('',#4221,1.);
#1255=VECTOR('',#4222,1.);
#1256=VECTOR('',#4223,1.);
#1257=VECTOR('',#4224,1.);
#1258=VECTOR('',#4227,1.);
#1259=VECTOR('',#4228,1.);
#1260=VECTOR('',#4229,1.);
#1261=VECTOR('',#4232,1.);
#1262=VECTOR('',#4233,1.);
#1263=VECTOR('',#4234,1.);
#1264=VECTOR('',#4237,1.);
#1265=VECTOR('',#4238,1.);
#1266=VECTOR('',#4239,1.);
#1267=VECTOR('',#4242,1.);
#1268=VECTOR('',#4243,1.);
#1269=VECTOR('',#4244,1.);
#1270=VECTOR('',#4247,1.);
#1271=VECTOR('',#4248,1.);
#1272=VECTOR('',#4265,0.475);
#1273=VECTOR('',#4270,0.5);
#1274=VECTOR('',#4275,0.485);
#1275=VECTOR('',#4284,0.31);
#1276=VECTOR('',#4287,0.3);
#1385=CIRCLE('',#3574,0.2942);
#1386=CIRCLE('',#3576,0.45);
#1387=CIRCLE('',#3578,0.5);
#1388=CIRCLE('',#3580,0.5);
#1389=CIRCLE('',#3582,0.47);
#1390=CIRCLE('',#3584,0.32);
#1391=CIRCLE('',#3586,0.2942);
#1614=VERTEX_POINT('',#5254);
#1615=VERTEX_POINT('',#5255);
#1616=VERTEX_POINT('',#5257);
#1617=VERTEX_POINT('',#5259);
#1618=VERTEX_POINT('',#5263);
#1619=VERTEX_POINT('',#5265);
#1620=VERTEX_POINT('',#5269);
#1621=VERTEX_POINT('',#5271);
#1622=VERTEX_POINT('',#5275);
#1623=VERTEX_POINT('',#5277);
#1624=VERTEX_POINT('',#5281);
#1625=VERTEX_POINT('',#5283);
#1626=VERTEX_POINT('',#5292);
#1627=VERTEX_POINT('',#5295);
#1628=VERTEX_POINT('',#5298);
#1629=VERTEX_POINT('',#5302);
#1630=VERTEX_POINT('',#5306);
#1631=VERTEX_POINT('',#5310);
#1632=VERTEX_POINT('',#5313);
#1920=EDGE_CURVE('',#1614,#1615,#1072,.T.);
#1921=EDGE_CURVE('',#1615,#1616,#1073,.T.);
#1922=EDGE_CURVE('',#1616,#1617,#1074,.T.);
#1923=EDGE_CURVE('',#1614,#1617,#1075,.T.);
#1924=EDGE_CURVE('',#1615,#1618,#1076,.T.);
#1925=EDGE_CURVE('',#1618,#1619,#1077,.T.);
#1926=EDGE_CURVE('',#1619,#1616,#1078,.T.);
#1927=EDGE_CURVE('',#1618,#1620,#1079,.T.);
#1928=EDGE_CURVE('',#1620,#1621,#1080,.T.);
#1929=EDGE_CURVE('',#1621,#1619,#1081,.T.);
#1930=EDGE_CURVE('',#1620,#1622,#1082,.T.);
#1931=EDGE_CURVE('',#1622,#1623,#1083,.T.);
#1932=EDGE_CURVE('',#1623,#1621,#1084,.T.);
#1933=EDGE_CURVE('',#1622,#1624,#1085,.T.);
#1934=EDGE_CURVE('',#1624,#1625,#1086,.T.);
#1935=EDGE_CURVE('',#1625,#1623,#1087,.T.);
#1936=EDGE_CURVE('',#1624,#1614,#1088,.T.);
#1937=EDGE_CURVE('',#1617,#1625,#1089,.T.);
#1938=EDGE_CURVE('',#1626,#1626,#1385,.T.);
#1939=EDGE_CURVE('',#1627,#1627,#1386,.T.);
#1940=EDGE_CURVE('',#1628,#1628,#1387,.T.);
#1941=EDGE_CURVE('',#1628,#1627,#1090,.T.);
#1942=EDGE_CURVE('',#1629,#1629,#1388,.T.);
#1943=EDGE_CURVE('',#1629,#1628,#1091,.T.);
#1944=EDGE_CURVE('',#1630,#1630,#1389,.T.);
#1945=EDGE_CURVE('',#1630,#1629,#1092,.T.);
#1946=EDGE_CURVE('',#1631,#1631,#1390,.T.);
#1947=EDGE_CURVE('',#1632,#1632,#1391,.F.);
#1948=EDGE_CURVE('',#1632,#1631,#1093,.T.);
#1949=EDGE_CURVE('',#1626,#1632,#1094,.T.);
#2436=ORIENTED_EDGE('',*,*,#1920,.T.);
#2437=ORIENTED_EDGE('',*,*,#1921,.T.);
#2438=ORIENTED_EDGE('',*,*,#1922,.T.);
#2439=ORIENTED_EDGE('',*,*,#1923,.F.);
#2440=ORIENTED_EDGE('',*,*,#1924,.T.);
#2441=ORIENTED_EDGE('',*,*,#1925,.T.);
#2442=ORIENTED_EDGE('',*,*,#1926,.T.);
#2443=ORIENTED_EDGE('',*,*,#1921,.F.);
#2444=ORIENTED_EDGE('',*,*,#1927,.T.);
#2445=ORIENTED_EDGE('',*,*,#1928,.T.);
#2446=ORIENTED_EDGE('',*,*,#1929,.T.);
#2447=ORIENTED_EDGE('',*,*,#1925,.F.);
#2448=ORIENTED_EDGE('',*,*,#1930,.T.);
#2449=ORIENTED_EDGE('',*,*,#1931,.T.);
#2450=ORIENTED_EDGE('',*,*,#1932,.T.);
#2451=ORIENTED_EDGE('',*,*,#1928,.F.);
#2452=ORIENTED_EDGE('',*,*,#1933,.T.);
#2453=ORIENTED_EDGE('',*,*,#1934,.T.);
#2454=ORIENTED_EDGE('',*,*,#1935,.T.);
#2455=ORIENTED_EDGE('',*,*,#1931,.F.);
#2456=ORIENTED_EDGE('',*,*,#1936,.T.);
#2457=ORIENTED_EDGE('',*,*,#1923,.T.);
#2458=ORIENTED_EDGE('',*,*,#1937,.T.);
#2459=ORIENTED_EDGE('',*,*,#1934,.F.);
#2460=ORIENTED_EDGE('',*,*,#1936,.F.);
#2461=ORIENTED_EDGE('',*,*,#1933,.F.);
#2462=ORIENTED_EDGE('',*,*,#1930,.F.);
#2463=ORIENTED_EDGE('',*,*,#1927,.F.);
#2464=ORIENTED_EDGE('',*,*,#1924,.F.);
#2465=ORIENTED_EDGE('',*,*,#1920,.F.);
#2466=ORIENTED_EDGE('',*,*,#1937,.F.);
#2467=ORIENTED_EDGE('',*,*,#1922,.F.);
#2468=ORIENTED_EDGE('',*,*,#1926,.F.);
#2469=ORIENTED_EDGE('',*,*,#1929,.F.);
#2470=ORIENTED_EDGE('',*,*,#1932,.F.);
#2471=ORIENTED_EDGE('',*,*,#1935,.F.);
#2472=ORIENTED_EDGE('',*,*,#1938,.F.);
#2473=ORIENTED_EDGE('',*,*,#1939,.F.);
#2474=ORIENTED_EDGE('',*,*,#1940,.F.);
#2475=ORIENTED_EDGE('',*,*,#1941,.T.);
#2476=ORIENTED_EDGE('',*,*,#1939,.T.);
#2477=ORIENTED_EDGE('',*,*,#1941,.F.);
#2478=ORIENTED_EDGE('',*,*,#1942,.F.);
#2479=ORIENTED_EDGE('',*,*,#1943,.T.);
#2480=ORIENTED_EDGE('',*,*,#1940,.T.);
#2481=ORIENTED_EDGE('',*,*,#1943,.F.);
#2482=ORIENTED_EDGE('',*,*,#1944,.F.);
#2483=ORIENTED_EDGE('',*,*,#1945,.T.);
#2484=ORIENTED_EDGE('',*,*,#1942,.T.);
#2485=ORIENTED_EDGE('',*,*,#1945,.F.);
#2486=ORIENTED_EDGE('',*,*,#1944,.T.);
#2487=ORIENTED_EDGE('',*,*,#1946,.F.);
#2488=ORIENTED_EDGE('',*,*,#1947,.F.);
#2489=ORIENTED_EDGE('',*,*,#1948,.T.);
#2490=ORIENTED_EDGE('',*,*,#1946,.T.);
#2491=ORIENTED_EDGE('',*,*,#1948,.F.);
#2492=ORIENTED_EDGE('',*,*,#1938,.T.);
#2493=ORIENTED_EDGE('',*,*,#1949,.T.);
#2494=ORIENTED_EDGE('',*,*,#1947,.T.);
#2495=ORIENTED_EDGE('',*,*,#1949,.F.);
#2949=CYLINDRICAL_SURFACE('',#3579,0.5);
#2950=CYLINDRICAL_SURFACE('',#3587,0.2942);
#3058=ADVANCED_FACE('',(#583),#463,.F.);
#3059=ADVANCED_FACE('',(#584),#464,.F.);
#3060=ADVANCED_FACE('',(#585),#465,.F.);
#3061=ADVANCED_FACE('',(#586),#466,.F.);
#3062=ADVANCED_FACE('',(#587),#467,.F.);
#3063=ADVANCED_FACE('',(#588),#468,.F.);
#3064=ADVANCED_FACE('',(#589),#469,.F.);
#3065=ADVANCED_FACE('',(#590),#470,.F.);
#3066=ADVANCED_FACE('',(#591),#471,.F.);
#3067=ADVANCED_FACE('',(#592),#472,.T.);
#3068=ADVANCED_FACE('',(#593),#223,.T.);
#3069=ADVANCED_FACE('',(#594),#2949,.T.);
#3070=ADVANCED_FACE('',(#595),#224,.T.);
#3071=ADVANCED_FACE('',(#596,#368),#473,.T.);
#3072=ADVANCED_FACE('',(#597),#225,.T.);
#3073=ADVANCED_FACE('',(#598),#2950,.T.);
#3190=CLOSED_SHELL('',(#3058,#3059,#3060,#3061,#3062,#3063,#3064,#3065));
#3191=CLOSED_SHELL('',(#3066,#3067,#3068,#3069,#3070,#3071,#3072,#3073));
#3564=AXIS2_PLACEMENT_3D('',#5252,#4217,#4218);
#3565=AXIS2_PLACEMENT_3D('',#5253,#4219,#4220);
#3566=AXIS2_PLACEMENT_3D('',#5262,#4225,#4226);
#3567=AXIS2_PLACEMENT_3D('',#5268,#4230,#4231);
#3568=AXIS2_PLACEMENT_3D('',#5274,#4235,#4236);
#3569=AXIS2_PLACEMENT_3D('',#5280,#4240,#4241);
#3570=AXIS2_PLACEMENT_3D('',#5286,#4245,#4246);
#3571=AXIS2_PLACEMENT_3D('',#5289,#4249,#4250);
#3572=AXIS2_PLACEMENT_3D('',#5290,#4251,#4252);
#3573=AXIS2_PLACEMENT_3D('',#5291,#4253,#4254);
#3574=AXIS2_PLACEMENT_3D('',#5293,#4255,#4256);
#3575=AXIS2_PLACEMENT_3D('',#5294,#4257,#4258);
#3576=AXIS2_PLACEMENT_3D('',#5296,#4259,#4260);
#3577=AXIS2_PLACEMENT_3D('',#5297,#4261,#4262);
#3578=AXIS2_PLACEMENT_3D('',#5299,#4263,#4264);
#3579=AXIS2_PLACEMENT_3D('',#5301,#4266,#4267);
#3580=AXIS2_PLACEMENT_3D('',#5303,#4268,#4269);
#3581=AXIS2_PLACEMENT_3D('',#5305,#4271,#4272);
#3582=AXIS2_PLACEMENT_3D('',#5307,#4273,#4274);
#3583=AXIS2_PLACEMENT_3D('',#5309,#4276,#4277);
#3584=AXIS2_PLACEMENT_3D('',#5311,#4278,#4279);
#3585=AXIS2_PLACEMENT_3D('',#5312,#4280,#4281);
#3586=AXIS2_PLACEMENT_3D('',#5314,#4282,#4283);
#3587=AXIS2_PLACEMENT_3D('',#5316,#4285,#4286);
#4217=DIRECTION('axis',(0.,0.,1.));
#4218=DIRECTION('refdir',(1.,0.,0.));
#4219=DIRECTION('center_axis',(0.866025403784439,0.,-0.5));
#4220=DIRECTION('ref_axis',(0.5,0.,0.866025403784439));
#4221=DIRECTION('',(-0.5,0.,-0.866025403784439));
#4222=DIRECTION('',(0.,-1.,0.));
#4223=DIRECTION('',(0.5,0.,0.866025403784439));
#4224=DIRECTION('',(0.,-1.,0.));
#4225=DIRECTION('center_axis',(1.92296268638356E-16,0.,-1.));
#4226=DIRECTION('ref_axis',(1.,0.,1.92296268638356E-16));
#4227=DIRECTION('',(-1.,0.,-1.92296268638356E-16));
#4228=DIRECTION('',(0.,-1.,0.));
#4229=DIRECTION('',(1.,0.,1.92296268638356E-16));
#4230=DIRECTION('center_axis',(-0.866025403784439,0.,-0.5));
#4231=DIRECTION('ref_axis',(0.5,0.,-0.866025403784439));
#4232=DIRECTION('',(-0.5,0.,0.866025403784438));
#4233=DIRECTION('',(0.,-1.,0.));
#4234=DIRECTION('',(0.5,0.,-0.866025403784438));
#4235=DIRECTION('center_axis',(-0.866025403784439,0.,0.5));
#4236=DIRECTION('ref_axis',(-0.5,0.,-0.866025403784439));
#4237=DIRECTION('',(0.5,0.,0.866025403784439));
#4238=DIRECTION('',(0.,-1.,0.));
#4239=DIRECTION('',(-0.5,0.,-0.866025403784439));
#4240=DIRECTION('center_axis',(-1.92296268638356E-16,0.,1.));
#4241=DIRECTION('ref_axis',(-1.,0.,-1.92296268638356E-16));
#4242=DIRECTION('',(1.,0.,1.92296268638356E-16));
#4243=DIRECTION('',(0.,-1.,0.));
#4244=DIRECTION('',(-1.,0.,-1.92296268638356E-16));
#4245=DIRECTION('center_axis',(0.866025403784439,0.,0.5));
#4246=DIRECTION('ref_axis',(-0.5,0.,0.866025403784439));
#4247=DIRECTION('',(0.5,0.,-0.866025403784439));
#4248=DIRECTION('',(-0.5,0.,0.866025403784439));
#4249=DIRECTION('center_axis',(0.,1.,0.));
#4250=DIRECTION('ref_axis',(1.,0.,0.));
#4251=DIRECTION('center_axis',(0.,-1.,0.));
#4252=DIRECTION('ref_axis',(0.,0.,-1.));
#4253=DIRECTION('center_axis',(0.,1.,0.));
#4254=DIRECTION('ref_axis',(1.,0.,0.));
#4255=DIRECTION('center_axis',(0.,1.,0.));
#4256=DIRECTION('ref_axis',(1.,0.,0.));
#4257=DIRECTION('center_axis',(0.,1.,0.));
#4258=DIRECTION('ref_axis',(0.,0.,1.));
#4259=DIRECTION('center_axis',(0.,-1.,0.));
#4260=DIRECTION('ref_axis',(1.,0.,0.));
#4261=DIRECTION('center_axis',(0.,-1.,0.));
#4262=DIRECTION('ref_axis',(1.,0.,0.));
#4263=DIRECTION('center_axis',(0.,-1.,0.));
#4264=DIRECTION('ref_axis',(1.,0.,0.));
#4265=DIRECTION('',(0.707106781186548,0.707106781186547,8.65956056235494E-17));
#4266=DIRECTION('center_axis',(0.,-1.,0.));
#4267=DIRECTION('ref_axis',(1.,0.,0.));
#4268=DIRECTION('center_axis',(0.,-1.,0.));
#4269=DIRECTION('ref_axis',(1.,0.,0.));
#4270=DIRECTION('',(0.,1.,0.));
#4271=DIRECTION('center_axis',(0.,1.,0.));
#4272=DIRECTION('ref_axis',(1.,0.,0.));
#4273=DIRECTION('center_axis',(0.,-1.,0.));
#4274=DIRECTION('ref_axis',(1.,0.,0.));
#4275=DIRECTION('',(-0.707106781186547,0.707106781186548,-8.65956056235493E-17));
#4276=DIRECTION('center_axis',(0.,-1.,0.));
#4277=DIRECTION('ref_axis',(0.,0.,-1.));
#4278=DIRECTION('center_axis',(0.,-1.,0.));
#4279=DIRECTION('ref_axis',(1.,0.,0.));
#4280=DIRECTION('center_axis',(0.,1.,0.));
#4281=DIRECTION('ref_axis',(1.,0.,0.));
#4282=DIRECTION('center_axis',(0.,1.,0.));
#4283=DIRECTION('ref_axis',(1.,0.,0.));
#4284=DIRECTION('',(-0.447213595499958,0.894427190999916,-5.47678698264203E-17));
#4285=DIRECTION('center_axis',(0.,-1.,0.));
#4286=DIRECTION('ref_axis',(1.,0.,0.));
#4287=DIRECTION('',(0.,1.,0.));
#5252=CARTESIAN_POINT('',(0.,0.,0.));
#5253=CARTESIAN_POINT('Origin',(0.144337567297406,-0.6,-0.25));
#5254=CARTESIAN_POINT('',(0.288675134594813,-0.6,0.));
#5255=CARTESIAN_POINT('',(0.144337567297406,-0.6,-0.25));
#5256=CARTESIAN_POINT('',(0.288675134594813,-0.6,0.));
#5257=CARTESIAN_POINT('',(0.144337567297406,-0.96,-0.25));
#5258=CARTESIAN_POINT('',(0.144337567297406,-0.6,-0.25));
#5259=CARTESIAN_POINT('',(0.288675134594813,-0.96,0.));
#5260=CARTESIAN_POINT('',(0.288675134594813,-0.96,0.));
#5261=CARTESIAN_POINT('',(0.288675134594813,-0.6,0.));
#5262=CARTESIAN_POINT('Origin',(-0.144337567297406,-0.6,-0.25));
#5263=CARTESIAN_POINT('',(-0.144337567297406,-0.6,-0.25));
#5264=CARTESIAN_POINT('',(0.144337567297406,-0.6,-0.25));
#5265=CARTESIAN_POINT('',(-0.144337567297406,-0.96,-0.25));
#5266=CARTESIAN_POINT('',(-0.144337567297406,-0.6,-0.25));
#5267=CARTESIAN_POINT('',(0.144337567297406,-0.96,-0.25));
#5268=CARTESIAN_POINT('Origin',(-0.288675134594813,-0.6,-8.32667268468867E-17));
#5269=CARTESIAN_POINT('',(-0.288675134594813,-0.6,-3.53525079574969E-17));
#5270=CARTESIAN_POINT('',(-0.144337567297406,-0.6,-0.25));
#5271=CARTESIAN_POINT('',(-0.288675134594813,-0.96,-5.55111512312578E-17));
#5272=CARTESIAN_POINT('',(-0.288675134594813,-0.6,-3.53525079574969E-17));
#5273=CARTESIAN_POINT('',(-0.144337567297406,-0.96,-0.25));
#5274=CARTESIAN_POINT('Origin',(-0.144337567297407,-0.6,0.25));
#5275=CARTESIAN_POINT('',(-0.144337567297407,-0.6,0.25));
#5276=CARTESIAN_POINT('',(-0.288675134594813,-0.6,-3.53525079574969E-17));
#5277=CARTESIAN_POINT('',(-0.144337567297407,-0.96,0.25));
#5278=CARTESIAN_POINT('',(-0.144337567297407,-0.6,0.25));
#5279=CARTESIAN_POINT('',(-0.288675134594813,-0.96,-3.53525079574969E-17));
#5280=CARTESIAN_POINT('Origin',(0.144337567297406,-0.6,0.25));
#5281=CARTESIAN_POINT('',(0.144337567297406,-0.6,0.25));
#5282=CARTESIAN_POINT('',(-0.144337567297407,-0.6,0.25));
#5283=CARTESIAN_POINT('',(0.144337567297406,-0.96,0.25));
#5284=CARTESIAN_POINT('',(0.144337567297406,-0.6,0.25));
#5285=CARTESIAN_POINT('',(-0.144337567297407,-0.96,0.25));
#5286=CARTESIAN_POINT('Origin',(0.288675134594813,-0.6,0.));
#5287=CARTESIAN_POINT('',(0.144337567297406,-0.6,0.25));
#5288=CARTESIAN_POINT('',(0.144337567297406,-0.96,0.25));
#5289=CARTESIAN_POINT('Origin',(0.,-0.6,0.));
#5290=CARTESIAN_POINT('Origin',(0.,-0.96,0.));
#5291=CARTESIAN_POINT('Origin',(0.,-1.8,0.));
#5292=CARTESIAN_POINT('',(-0.2942,-1.8,3.60291088309151E-17));
#5293=CARTESIAN_POINT('Origin',(0.,-1.8,0.));
#5294=CARTESIAN_POINT('Origin',(0.45,0.6,0.));
#5295=CARTESIAN_POINT('',(-0.45,0.6,-5.51091059616309E-17));
#5296=CARTESIAN_POINT('Origin',(0.,0.6,0.));
#5297=CARTESIAN_POINT('Origin',(0.,0.575,0.));
#5298=CARTESIAN_POINT('',(-0.5,0.55,-6.12323399573677E-17));
#5299=CARTESIAN_POINT('Origin',(0.,0.55,0.));
#5300=CARTESIAN_POINT('',(-0.475,0.575,-5.81707229594993E-17));
#5301=CARTESIAN_POINT('Origin',(0.,0.29,0.));
#5302=CARTESIAN_POINT('',(-0.5,0.0299999999999998,-6.12323399573677E-17));
#5303=CARTESIAN_POINT('Origin',(0.,0.0299999999999998,0.));
#5304=CARTESIAN_POINT('',(-0.5,0.29,-6.12323399573677E-17));
#5305=CARTESIAN_POINT('Origin',(0.,0.0150000000000001,0.));
#5306=CARTESIAN_POINT('',(-0.47,7.11236625150491E-17,-5.75583995599256E-17));
#5307=CARTESIAN_POINT('Origin',(0.,0.,0.));
#5308=CARTESIAN_POINT('',(-0.485,0.0150000000000001,-5.93953697586466E-17));
#5309=CARTESIAN_POINT('Origin',(0.32,0.,0.));
#5310=CARTESIAN_POINT('',(-0.32,-6.93889390390723E-18,-3.91886975727153E-17));
#5311=CARTESIAN_POINT('Origin',(0.,0.,0.));
#5312=CARTESIAN_POINT('Origin',(0.,-0.02,0.));
#5313=CARTESIAN_POINT('',(-0.2942,-0.0515999999999999,3.60291088309151E-17));
#5314=CARTESIAN_POINT('Origin',(0.,-0.0515999999999999,0.));
#5315=CARTESIAN_POINT('',(-0.31,-0.02,-3.7964050773568E-17));
#5316=CARTESIAN_POINT('Origin',(0.,-1.24,0.));
#5317=CARTESIAN_POINT('',(-0.2942,-1.24,-3.60291088309151E-17));
#6200=UNCERTAINTY_MEASURE_WITH_UNIT(LENGTH_MEASURE(0.001),#6242,
'DISTANCE_ACCURACY_VALUE',
'Maximum model space distance between geometric entities at asserted c
onnectivities');
#6215=UNCERTAINTY_MEASURE_WITH_UNIT(LENGTH_MEASURE(0.001),#6242,
'DISTANCE_ACCURACY_VALUE',
'Maximum model space distance between geometric entities at asserted c
onnectivities');
#6226=(
GEOMETRIC_REPRESENTATION_CONTEXT(3)
GLOBAL_UNCERTAINTY_ASSIGNED_CONTEXT((#6200))
GLOBAL_UNIT_ASSIGNED_CONTEXT((#6242,#6244,#6245))
REPRESENTATION_CONTEXT('','3D')
);
#6241=(
GEOMETRIC_REPRESENTATION_CONTEXT(3)
GLOBAL_UNCERTAINTY_ASSIGNED_CONTEXT((#6215))
GLOBAL_UNIT_ASSIGNED_CONTEXT((#6242,#6244,#6245))
REPRESENTATION_CONTEXT('','3D')
);
#6242=(
LENGTH_UNIT()
NAMED_UNIT(*)
SI_UNIT(.CENTI.,.METRE.)
);
#6244=(
NAMED_UNIT(*)
PLANE_ANGLE_UNIT()
SI_UNIT($,.RADIAN.)
);
#6245=(
NAMED_UNIT(*)
SI_UNIT($,.STERADIAN.)
SOLID_ANGLE_UNIT()
);
#6256=SHAPE_DEFINITION_REPRESENTATION(#6281,#6350);
#6281=PRODUCT_DEFINITION_SHAPE('',$,#6376);
#6350=SHAPE_REPRESENTATION('',(#3564),#6226);
#6365=PRODUCT_DEFINITION_CONTEXT('part definition',#6442,'design');
#6376=PRODUCT_DEFINITION('M6x18 mounting screw','M6x18 mounting screw',
#6401,#6365);
#6401=PRODUCT_DEFINITION_FORMATION('',$,#6454);
#6442=APPLICATION_CONTEXT(
'Core Data for Automotive Mechanical Design Process');
#6443=PRODUCT_CONTEXT('part definition',#6442,'mechanical');
#6454=PRODUCT('M6x18 mounting screw','M6x18 mounting screw',
'M6x18 mounting screw',(#6443));
#6539=COLOUR_RGB('Black',0.12,0.14,0.17);
#6540=FILL_AREA_STYLE_COLOUR('',#6539);
#6541=FILL_AREA_STYLE('',(#6540));
#6542=SURFACE_STYLE_FILL_AREA(#6541);
#6543=SURFACE_SIDE_STYLE('',(#6542));
#6544=SURFACE_STYLE_USAGE(.BOTH.,#6543);
#6545=PRESENTATION_STYLE_ASSIGNMENT((#6544));
ENDSEC;
END-ISO-10303-21;
